ISO-10303-21;
HEADER;
/* Generated by software containing ST-Developer
 * from STEP Tools, Inc. (www.steptools.com) 
 */

FILE_DESCRIPTION(
/* description */ ('STEP AP214'),
/* implementation_level */ '2;1');

FILE_NAME(
/* name */ 'Eye Bolt.step',
/* time_stamp */ '2026-11-14T05:56:09-08:00',
/* author */ (''),
/* organization */ (''),
/* preprocessor_version */ 'ST-DEVELOPER v20.2',
/* originating_system */ 'Autodesk Translation Framework v15.17.0.0',
/* authorisation */ '');

FILE_SCHEMA (('AUTOMOTIVE_DESIGN { 1 0 10303 214 3 1 1 }'));
ENDSEC;

DATA;
#10=MECHANICAL_DESIGN_GEOMETRIC_PRESENTATION_REPRESENTATION('',(#102),#3207);
#90=SHAPE_REPRESENTATION_RELATIONSHIP('SRR','None',#3242,#96);
#96=ADVANCED_BREP_SHAPE_REPRESENTATION('',(#108),#3201);
#102=STYLED_ITEM('',(#3281),#108);
#108=MANIFOLD_SOLID_BREP('Body1',#1280);
#114=PLANE('',#1365);
#115=PLANE('',#1366);
#116=PLANE('',#1367);
#117=PLANE('',#1368);
#118=PLANE('',#1369);
#119=PLANE('',#1370);
#120=PLANE('',#1371);
#152=LINE('',#1980,#219);
#153=LINE('',#1985,#220);
#154=LINE('',#1987,#221);
#155=LINE('',#1988,#222);
#156=LINE('',#1991,#223);
#157=LINE('',#1993,#224);
#158=LINE('',#1994,#225);
#159=LINE('',#1996,#226);
#160=LINE('',#1997,#227);
#161=LINE('',#1999,#228);
#162=LINE('',#2001,#229);
#219=VECTOR('',#1538,4.);
#220=VECTOR('',#1545,1000.);
#221=VECTOR('',#1546,1000.);
#222=VECTOR('',#1547,1000.);
#223=VECTOR('',#1550,1000.);
#224=VECTOR('',#1551,1000.);
#225=VECTOR('',#1552,1000.);
#226=VECTOR('',#1555,1000.);
#227=VECTOR('',#1556,1000.);
#228=VECTOR('',#1559,1000.);
#229=VECTOR('',#1562,1000.);
#286=CYLINDRICAL_SURFACE('',#1360,4.);
#309=FACE_BOUND('',#423,.T.);
#328=B_SPLINE_CURVE_WITH_KNOTS('',3,(#1923,#1924,#1925,#1926,#1927,#1928,
#1929,#1930,#1931,#1932,#1933,#1934,#1935,#1936,#1937,#1938,#1939,#1940,
#1941,#1942,#1943,#1944,#1945),.UNSPECIFIED.,.F.,.F.,(4,2,2,2,2,3,2,2,2,
2,4),(-0.44021020401708,-0.36937623196026,-0.276548406644596,-0.183720581328932,
-0.0918602906644662,0.,0.0918602906644663,0.183720581328932,0.276548406644596,
0.36937623196026,0.440210204017081),.UNSPECIFIED.);
#329=B_SPLINE_CURVE_WITH_KNOTS('',3,(#1949,#1950,#1951,#1952,#1953,#1954,
#1955,#1956,#1957,#1958,#1959,#1960,#1961,#1962,#1963,#1964,#1965,#1966,
#1967,#1968,#1969,#1970,#1971),.UNSPECIFIED.,.F.,.F.,(4,2,2,2,2,3,2,2,2,
2,4),(2.57327484364004,2.64410881569686,2.73693664101252,2.82976446632818,
2.92162475699265,3.01348504765712,3.10534533832158,3.19720562898605,3.29003345430171,
3.38286127961738,3.4536952516742),.UNSPECIFIED.);
#346=FACE_OUTER_BOUND('',#422,.T.);
#347=FACE_OUTER_BOUND('',#424,.T.);
#348=FACE_OUTER_BOUND('',#425,.T.);
#349=FACE_OUTER_BOUND('',#426,.T.);
#350=FACE_OUTER_BOUND('',#427,.T.);
#351=FACE_OUTER_BOUND('',#428,.T.);
#352=FACE_OUTER_BOUND('',#429,.T.);
#353=FACE_OUTER_BOUND('',#430,.T.);
#354=FACE_OUTER_BOUND('',#431,.T.);
#422=EDGE_LOOP('',(#861,#862,#863,#864));
#423=EDGE_LOOP('',(#865,#866,#867,#868));
#424=EDGE_LOOP('',(#869,#870,#871,#872,#873,#874));
#425=EDGE_LOOP('',(#875,#876,#877,#878));
#426=EDGE_LOOP('',(#879,#880,#881,#882,#883));
#427=EDGE_LOOP('',(#884,#885,#886,#887));
#428=EDGE_LOOP('',(#888,#889,#890,#891,#892));
#429=EDGE_LOOP('',(#893,#894,#895,#896));
#430=EDGE_LOOP('',(#897,#898,#899,#900,#901));
#431=EDGE_LOOP('',(#902));
#517=CIRCLE('',#1356,5.);
#518=CIRCLE('',#1357,15.);
#519=CIRCLE('',#1358,23.);
#520=CIRCLE('',#1359,23.);
#521=CIRCLE('',#1361,4.);
#522=CIRCLE('',#1362,4.);
#523=CIRCLE('',#1363,4.);
#524=CIRCLE('',#1364,4.);
#586=VERTEX_POINT('',#1918);
#587=VERTEX_POINT('',#1921);
#588=VERTEX_POINT('',#1922);
#589=VERTEX_POINT('',#1946);
#590=VERTEX_POINT('',#1948);
#591=VERTEX_POINT('',#1974);
#592=VERTEX_POINT('',#1975);
#593=VERTEX_POINT('',#1977);
#594=VERTEX_POINT('',#1979);
#595=VERTEX_POINT('',#1984);
#596=VERTEX_POINT('',#1986);
#597=VERTEX_POINT('',#1990);
#598=VERTEX_POINT('',#1992);
#694=EDGE_CURVE('',#586,#586,#517,.T.);
#695=EDGE_CURVE('',#586,#586,#518,.T.);
#696=EDGE_CURVE('',#587,#588,#328,.T.);
#697=EDGE_CURVE('',#589,#587,#519,.T.);
#698=EDGE_CURVE('',#590,#589,#329,.F.);
#699=EDGE_CURVE('',#588,#590,#520,.T.);
#700=EDGE_CURVE('',#591,#592,#521,.T.);
#701=EDGE_CURVE('',#592,#593,#522,.T.);
#702=EDGE_CURVE('',#593,#594,#152,.T.);
#703=EDGE_CURVE('',#594,#594,#523,.T.);
#704=EDGE_CURVE('',#593,#591,#524,.T.);
#705=EDGE_CURVE('',#595,#591,#153,.T.);
#706=EDGE_CURVE('',#596,#595,#154,.T.);
#707=EDGE_CURVE('',#592,#596,#155,.T.);
#708=EDGE_CURVE('',#597,#592,#156,.T.);
#709=EDGE_CURVE('',#598,#597,#157,.T.);
#710=EDGE_CURVE('',#591,#598,#158,.T.);
#711=EDGE_CURVE('',#590,#595,#159,.T.);
#712=EDGE_CURVE('',#589,#596,#160,.T.);
#713=EDGE_CURVE('',#588,#598,#161,.T.);
#714=EDGE_CURVE('',#587,#597,#162,.T.);
#861=ORIENTED_EDGE('',*,*,#694,.F.);
#862=ORIENTED_EDGE('',*,*,#695,.T.);
#863=ORIENTED_EDGE('',*,*,#694,.T.);
#864=ORIENTED_EDGE('',*,*,#695,.F.);
#865=ORIENTED_EDGE('',*,*,#696,.F.);
#866=ORIENTED_EDGE('',*,*,#697,.F.);
#867=ORIENTED_EDGE('',*,*,#698,.F.);
#868=ORIENTED_EDGE('',*,*,#699,.F.);
#869=ORIENTED_EDGE('',*,*,#700,.T.);
#870=ORIENTED_EDGE('',*,*,#701,.T.);
#871=ORIENTED_EDGE('',*,*,#702,.T.);
#872=ORIENTED_EDGE('',*,*,#703,.F.);
#873=ORIENTED_EDGE('',*,*,#702,.F.);
#874=ORIENTED_EDGE('',*,*,#704,.T.);
#875=ORIENTED_EDGE('',*,*,#700,.F.);
#876=ORIENTED_EDGE('',*,*,#705,.F.);
#877=ORIENTED_EDGE('',*,*,#706,.F.);
#878=ORIENTED_EDGE('',*,*,#707,.F.);
#879=ORIENTED_EDGE('',*,*,#701,.F.);
#880=ORIENTED_EDGE('',*,*,#708,.F.);
#881=ORIENTED_EDGE('',*,*,#709,.F.);
#882=ORIENTED_EDGE('',*,*,#710,.F.);
#883=ORIENTED_EDGE('',*,*,#704,.F.);
#884=ORIENTED_EDGE('',*,*,#711,.F.);
#885=ORIENTED_EDGE('',*,*,#698,.T.);
#886=ORIENTED_EDGE('',*,*,#712,.T.);
#887=ORIENTED_EDGE('',*,*,#706,.T.);
#888=ORIENTED_EDGE('',*,*,#713,.F.);
#889=ORIENTED_EDGE('',*,*,#699,.T.);
#890=ORIENTED_EDGE('',*,*,#711,.T.);
#891=ORIENTED_EDGE('',*,*,#705,.T.);
#892=ORIENTED_EDGE('',*,*,#710,.T.);
#893=ORIENTED_EDGE('',*,*,#714,.F.);
#894=ORIENTED_EDGE('',*,*,#696,.T.);
#895=ORIENTED_EDGE('',*,*,#713,.T.);
#896=ORIENTED_EDGE('',*,*,#709,.T.);
#897=ORIENTED_EDGE('',*,*,#712,.F.);
#898=ORIENTED_EDGE('',*,*,#697,.T.);
#899=ORIENTED_EDGE('',*,*,#714,.T.);
#900=ORIENTED_EDGE('',*,*,#708,.T.);
#901=ORIENTED_EDGE('',*,*,#707,.T.);
#902=ORIENTED_EDGE('',*,*,#703,.T.);
#1195=TOROIDAL_SURFACE('',#1355,20.,5.);
#1204=ADVANCED_FACE('',(#346,#309),#1195,.T.);
#1205=ADVANCED_FACE('',(#347),#286,.T.);
#1206=ADVANCED_FACE('',(#348),#114,.F.);
#1207=ADVANCED_FACE('',(#349),#115,.F.);
#1208=ADVANCED_FACE('',(#350),#116,.F.);
#1209=ADVANCED_FACE('',(#351),#117,.F.);
#1210=ADVANCED_FACE('',(#352),#118,.F.);
#1211=ADVANCED_FACE('',(#353),#119,.F.);
#1212=ADVANCED_FACE('',(#354),#120,.T.);
#1280=CLOSED_SHELL('',(#1204,#1205,#1206,#1207,#1208,#1209,#1210,#1211,
#1212));
#1354=AXIS2_PLACEMENT_3D('',#1916,#1520,#1521);
#1355=AXIS2_PLACEMENT_3D('',#1917,#1522,#1523);
#1356=AXIS2_PLACEMENT_3D('',#1919,#1524,#1525);
#1357=AXIS2_PLACEMENT_3D('',#1920,#1526,#1527);
#1358=AXIS2_PLACEMENT_3D('',#1947,#1528,#1529);
#1359=AXIS2_PLACEMENT_3D('',#1972,#1530,#1531);
#1360=AXIS2_PLACEMENT_3D('',#1973,#1532,#1533);
#1361=AXIS2_PLACEMENT_3D('',#1976,#1534,#1535);
#1362=AXIS2_PLACEMENT_3D('',#1978,#1536,#1537);
#1363=AXIS2_PLACEMENT_3D('',#1981,#1539,#1540);
#1364=AXIS2_PLACEMENT_3D('',#1982,#1541,#1542);
#1365=AXIS2_PLACEMENT_3D('',#1983,#1543,#1544);
#1366=AXIS2_PLACEMENT_3D('',#1989,#1548,#1549);
#1367=AXIS2_PLACEMENT_3D('',#1995,#1553,#1554);
#1368=AXIS2_PLACEMENT_3D('',#1998,#1557,#1558);
#1369=AXIS2_PLACEMENT_3D('',#2000,#1560,#1561);
#1370=AXIS2_PLACEMENT_3D('',#2002,#1563,#1564);
#1371=AXIS2_PLACEMENT_3D('',#2003,#1565,#1566);
#1520=DIRECTION('axis',(0.,0.,1.));
#1521=DIRECTION('refdir',(1.,0.,0.));
#1522=DIRECTION('center_axis',(-1.73472347597681E-16,1.,0.));
#1523=DIRECTION('ref_axis',(-1.,-1.73472347597681E-16,0.));
#1524=DIRECTION('center_axis',(-1.22464679914735E-16,-2.12442355226077E-32,
-1.));
#1525=DIRECTION('ref_axis',(1.,1.73472347597681E-16,-1.22464679914735E-16));
#1526=DIRECTION('center_axis',(1.73472347597681E-16,-1.,0.));
#1527=DIRECTION('ref_axis',(-1.,-1.73472347597681E-16,0.));
#1528=DIRECTION('center_axis',(0.,1.,0.));
#1529=DIRECTION('ref_axis',(0.,0.,1.));
#1530=DIRECTION('center_axis',(0.,-1.,0.));
#1531=DIRECTION('ref_axis',(0.,0.,-1.));
#1532=DIRECTION('center_axis',(0.,0.,1.));
#1533=DIRECTION('ref_axis',(1.,0.,0.));
#1534=DIRECTION('center_axis',(0.,0.,-1.));
#1535=DIRECTION('ref_axis',(-1.,0.,0.));
#1536=DIRECTION('center_axis',(0.,0.,-1.));
#1537=DIRECTION('ref_axis',(-1.,0.,0.));
#1538=DIRECTION('',(0.,0.,-1.));
#1539=DIRECTION('center_axis',(0.,0.,-1.));
#1540=DIRECTION('ref_axis',(-1.,0.,0.));
#1541=DIRECTION('center_axis',(0.,0.,-1.));
#1542=DIRECTION('ref_axis',(-1.,0.,0.));
#1543=DIRECTION('center_axis',(0.,0.,1.));
#1544=DIRECTION('ref_axis',(1.,0.,0.));
#1545=DIRECTION('',(-1.,0.,0.));
#1546=DIRECTION('',(0.,1.,0.));
#1547=DIRECTION('',(1.,0.,0.));
#1548=DIRECTION('center_axis',(0.,0.,1.));
#1549=DIRECTION('ref_axis',(1.,0.,0.));
#1550=DIRECTION('',(1.,0.,0.));
#1551=DIRECTION('',(0.,-1.,0.));
#1552=DIRECTION('',(-1.,0.,0.));
#1553=DIRECTION('center_axis',(-1.,0.,0.));
#1554=DIRECTION('ref_axis',(0.,0.,1.));
#1555=DIRECTION('',(0.,0.,-1.));
#1556=DIRECTION('',(0.,0.,-1.));
#1557=DIRECTION('center_axis',(0.,-1.,0.));
#1558=DIRECTION('ref_axis',(0.,0.,-1.));
#1559=DIRECTION('',(0.,0.,-1.));
#1560=DIRECTION('center_axis',(1.,0.,0.));
#1561=DIRECTION('ref_axis',(0.,0.,-1.));
#1562=DIRECTION('',(0.,0.,-1.));
#1563=DIRECTION('center_axis',(0.,1.,0.));
#1564=DIRECTION('ref_axis',(0.,0.,1.));
#1565=DIRECTION('center_axis',(0.,0.,-1.));
#1566=DIRECTION('ref_axis',(-1.,0.,0.));
#1916=CARTESIAN_POINT('',(0.,0.,0.));
#1917=CARTESIAN_POINT('Origin',(-20.,-3.46944695195361E-15,0.));
#1918=CARTESIAN_POINT('',(-5.,-2.55038338414727E-16,-1.83697019872103E-15));
#1919=CARTESIAN_POINT('Origin',(0.,-4.93038065763132E-31,-2.44929359829471E-15));
#1920=CARTESIAN_POINT('Origin',(-20.,-4.08177035152729E-15,0.));
#1921=CARTESIAN_POINT('',(-25.,-4.,-22.4499443206436));
#1922=CARTESIAN_POINT('',(-25.,4.,-22.4499443206436));
#1923=CARTESIAN_POINT('Ctrl Pts',(-25.,-3.99999999999891,-22.4499443206451));
#1924=CARTESIAN_POINT('Ctrl Pts',(-25.,-3.84867032046629,-22.6566609508832));
#1925=CARTESIAN_POINT('Ctrl Pts',(-25.,-3.6835445374341,-22.848437982591));
#1926=CARTESIAN_POINT('Ctrl Pts',(-25.,-3.300301175418,-23.2366874901609));
#1927=CARTESIAN_POINT('Ctrl Pts',(-25.,-3.04126350020025,-23.4558741060066));
#1928=CARTESIAN_POINT('Ctrl Pts',(-25.,-2.48262666767397,-23.8342495941587));
#1929=CARTESIAN_POINT('Ctrl Pts',(-25.,-2.18300887639722,-23.9934109543844));
#1930=CARTESIAN_POINT('Ctrl Pts',(-25.,-1.61519723056183,-24.2312903430839));
#1931=CARTESIAN_POINT('Ctrl Pts',(-25.,-1.29504313685635,-24.3324786024398));
#1932=CARTESIAN_POINT('Ctrl Pts',(-25.,-0.640546152188757,-24.464287836246));
#1933=CARTESIAN_POINT('Ctrl Pts',(-25.,-0.306200968881558,-24.4948974278318));
#1934=CARTESIAN_POINT('Ctrl Pts',(-25.,-4.31946145518225E-15,-24.4948974278318));
#1935=CARTESIAN_POINT('Ctrl Pts',(-25.,0.30620096888155,-24.4948974278318));
#1936=CARTESIAN_POINT('Ctrl Pts',(-25.,0.64054615218875,-24.464287836246));
#1937=CARTESIAN_POINT('Ctrl Pts',(-25.,1.29504313685634,-24.3324786024398));
#1938=CARTESIAN_POINT('Ctrl Pts',(-25.,1.61519723056182,-24.2312903430839));
#1939=CARTESIAN_POINT('Ctrl Pts',(-25.,2.18300887639721,-23.9934109543844));
#1940=CARTESIAN_POINT('Ctrl Pts',(-25.,2.48262666767396,-23.8342495941587));
#1941=CARTESIAN_POINT('Ctrl Pts',(-25.,3.04126350020024,-23.4558741060066));
#1942=CARTESIAN_POINT('Ctrl Pts',(-25.,3.30030117541799,-23.2366874901609));
#1943=CARTESIAN_POINT('Ctrl Pts',(-25.,3.68354453743409,-22.848437982591));
#1944=CARTESIAN_POINT('Ctrl Pts',(-25.,3.84867032046629,-22.6566609508832));
#1945=CARTESIAN_POINT('Ctrl Pts',(-25.,3.99999999999891,-22.4499443206451));
#1946=CARTESIAN_POINT('',(-15.,-4.,-22.4499443206436));
#1947=CARTESIAN_POINT('Origin',(-20.,-4.,0.));
#1948=CARTESIAN_POINT('',(-15.,4.,-22.4499443206436));
#1949=CARTESIAN_POINT('Ctrl Pts',(-15.,-3.99999999999891,-22.4499443206451));
#1950=CARTESIAN_POINT('Ctrl Pts',(-15.,-3.84867032046629,-22.6566609508833));
#1951=CARTESIAN_POINT('Ctrl Pts',(-15.,-3.68354453743409,-22.848437982591));
#1952=CARTESIAN_POINT('Ctrl Pts',(-15.,-3.30030117541799,-23.2366874901609));
#1953=CARTESIAN_POINT('Ctrl Pts',(-15.,-3.04126350020025,-23.4558741060066));
#1954=CARTESIAN_POINT('Ctrl Pts',(-15.,-2.48262666767397,-23.8342495941587));
#1955=CARTESIAN_POINT('Ctrl Pts',(-15.,-2.18300887639722,-23.9934109543844));
#1956=CARTESIAN_POINT('Ctrl Pts',(-15.,-1.61519723056182,-24.2312903430839));
#1957=CARTESIAN_POINT('Ctrl Pts',(-15.,-1.29504313685635,-24.3324786024398));
#1958=CARTESIAN_POINT('Ctrl Pts',(-15.,-0.640546152188757,-24.464287836246));
#1959=CARTESIAN_POINT('Ctrl Pts',(-15.,-0.306200968881557,-24.4948974278318));
#1960=CARTESIAN_POINT('Ctrl Pts',(-15.,-2.60208521396521E-15,-24.4948974278318));
#1961=CARTESIAN_POINT('Ctrl Pts',(-15.,0.306200968881551,-24.4948974278318));
#1962=CARTESIAN_POINT('Ctrl Pts',(-15.,0.64054615218875,-24.464287836246));
#1963=CARTESIAN_POINT('Ctrl Pts',(-15.,1.29504313685634,-24.3324786024398));
#1964=CARTESIAN_POINT('Ctrl Pts',(-15.,1.61519723056182,-24.2312903430839));
#1965=CARTESIAN_POINT('Ctrl Pts',(-15.,2.18300887639722,-23.9934109543844));
#1966=CARTESIAN_POINT('Ctrl Pts',(-15.,2.48262666767396,-23.8342495941587));
#1967=CARTESIAN_POINT('Ctrl Pts',(-15.,3.04126350020024,-23.4558741060066));
#1968=CARTESIAN_POINT('Ctrl Pts',(-15.,3.30030117541799,-23.2366874901609));
#1969=CARTESIAN_POINT('Ctrl Pts',(-15.,3.68354453743409,-22.848437982591));
#1970=CARTESIAN_POINT('Ctrl Pts',(-15.,3.84867032046629,-22.6566609508832));
#1971=CARTESIAN_POINT('Ctrl Pts',(-15.,3.99999999999891,-22.4499443206451));
#1972=CARTESIAN_POINT('Origin',(-20.,4.,0.));
#1973=CARTESIAN_POINT('Origin',(-20.,0.,-51.));
#1974=CARTESIAN_POINT('',(-20.,4.,-28.));
#1975=CARTESIAN_POINT('',(-20.,-4.,-28.));
#1976=CARTESIAN_POINT('Origin',(-20.,0.,-28.));
#1977=CARTESIAN_POINT('',(-24.,-4.89858719658941E-16,-28.));
#1978=CARTESIAN_POINT('Origin',(-20.,0.,-28.));
#1979=CARTESIAN_POINT('',(-24.,-4.89858719658941E-16,-51.));
#1980=CARTESIAN_POINT('',(-24.,-4.89858719658941E-16,-51.));
#1981=CARTESIAN_POINT('Origin',(-20.,0.,-51.));
#1982=CARTESIAN_POINT('Origin',(-20.,0.,-28.));
#1983=CARTESIAN_POINT('Origin',(0.,0.,-28.));
#1984=CARTESIAN_POINT('',(-15.,4.,-28.));
#1985=CARTESIAN_POINT('',(-15.,4.,-28.));
#1986=CARTESIAN_POINT('',(-15.,-4.,-28.));
#1987=CARTESIAN_POINT('',(-15.,0.,-28.));
#1988=CARTESIAN_POINT('',(-25.,-4.,-28.));
#1989=CARTESIAN_POINT('Origin',(0.,0.,-28.));
#1990=CARTESIAN_POINT('',(-25.,-4.,-28.));
#1991=CARTESIAN_POINT('',(-25.,-4.,-28.));
#1992=CARTESIAN_POINT('',(-25.,4.,-28.));
#1993=CARTESIAN_POINT('',(-25.,4.,-28.));
#1994=CARTESIAN_POINT('',(-15.,4.,-28.));
#1995=CARTESIAN_POINT('Origin',(-15.,0.,-18.));
#1996=CARTESIAN_POINT('',(-15.,4.,-18.));
#1997=CARTESIAN_POINT('',(-15.,-4.,-18.));
#1998=CARTESIAN_POINT('Origin',(-15.,4.,-18.));
#1999=CARTESIAN_POINT('',(-25.,4.,-18.));
#2000=CARTESIAN_POINT('Origin',(-25.,4.,-18.));
#2001=CARTESIAN_POINT('',(-25.,-4.,-18.));
#2002=CARTESIAN_POINT('Origin',(-25.,-4.,-18.));
#2003=CARTESIAN_POINT('Origin',(-20.,0.,-51.));
#3193=UNCERTAINTY_MEASURE_WITH_UNIT(LENGTH_MEASURE(0.01),#3208,
'DISTANCE_ACCURACY_VALUE',
'Maximum model space distance between geometric entities at asserted c
onnectivities');
#3199=UNCERTAINTY_MEASURE_WITH_UNIT(LENGTH_MEASURE(0.01),#3208,
'DISTANCE_ACCURACY_VALUE',
'Maximum model space distance between geometric entities at asserted c
onnectivities');
#3201=(
GEOMETRIC_REPRESENTATION_CONTEXT(3)
GLOBAL_UNCERTAINTY_ASSIGNED_CONTEXT((#3193))
GLOBAL_UNIT_ASSIGNED_CONTEXT((#3208,#3210,#3211))
REPRESENTATION_CONTEXT('','3D')
);
#3207=(
GEOMETRIC_REPRESENTATION_CONTEXT(3)
GLOBAL_UNCERTAINTY_ASSIGNED_CONTEXT((#3199))
GLOBAL_UNIT_ASSIGNED_CONTEXT((#3208,#3210,#3211))
REPRESENTATION_CONTEXT('','3D')
);
#3208=(
LENGTH_UNIT()
NAMED_UNIT(*)
SI_UNIT(.MILLI.,.METRE.)
);
#3210=(
NAMED_UNIT(*)
PLANE_ANGLE_UNIT()
SI_UNIT($,.RADIAN.)
);
#3211=(
NAMED_UNIT(*)
SI_UNIT($,.STERADIAN.)
SOLID_ANGLE_UNIT()
);
#3213=SHAPE_DEFINITION_REPRESENTATION(#3220,#3242);
#3220=PRODUCT_DEFINITION_SHAPE('',$,#3250);
#3242=SHAPE_REPRESENTATION('',(#1354),#3201);
#3248=PRODUCT_DEFINITION_CONTEXT('part definition',#3271,'design');
#3250=PRODUCT_DEFINITION('Eye Bolt','Eye Bolt',#3257,#3248);
#3257=PRODUCT_DEFINITION_FORMATION('',$,#3274);
#3271=APPLICATION_CONTEXT(
'Core Data for Automotive Mechanical Design Process');
#3272=PRODUCT_CONTEXT('part definition',#3271,'mechanical');
#3274=PRODUCT('Eye Bolt','Eye Bolt',$,(#3272));
#3281=PRESENTATION_STYLE_ASSIGNMENT((#3285));
#3285=SURFACE_STYLE_USAGE(.BOTH.,#3289);
#3289=SURFACE_SIDE_STYLE('',(#3293));
#3293=SURFACE_STYLE_FILL_AREA(#3297);
#3297=FILL_AREA_STYLE('Opaque(97,158,199)',(#3301));
#3301=FILL_AREA_STYLE_COLOUR('Opaque(97,158,199)',#3305);
#3305=COLOUR_RGB('Opaque(97,158,199)',0.380392156862745,0.619607843137255,
0.780392156862745);
ENDSEC;
END-ISO-10303-21;
